ISO-10303-21;
HEADER;
/* Generated by software containing ST-Developer
 * from STEP Tools, Inc. (www.steptools.com) 
 */

FILE_DESCRIPTION(
/* description */ ('STEP AP214'),
/* implementation_level */ '2;1');

FILE_NAME(
/* name */ 'Ball Screw Support Bracket.step',
/* time_stamp */ '2026-11-15T14:55:55-08:00',
/* author */ (''),
/* organization */ (''),
/* preprocessor_version */ 'ST-DEVELOPER v20.2',
/* originating_system */ 'Autodesk Translation Framework v15.17.0.0',
/* authorisation */ '');

FILE_SCHEMA (('AUTOMOTIVE_DESIGN { 1 0 10303 214 3 1 1 }'));
ENDSEC;

DATA;
#10=MECHANICAL_DESIGN_GEOMETRIC_PRESENTATION_REPRESENTATION('',(#944),#57079);
#884=SHAPE_REPRESENTATION_RELATIONSHIP('SRR','None',#57273,#913);
#913=ADVANCED_BREP_SHAPE_REPRESENTATION('',(#981),#57065);
#944=STYLED_ITEM('',(#57444),#981);
#981=MANIFOLD_SOLID_BREP('Body1',#24544);
#1157=FACE_BOUND('',#4327,.T.);
#1158=FACE_BOUND('',#4328,.T.);
#1159=FACE_BOUND('',#4329,.T.);
#1160=FACE_BOUND('',#4330,.T.);
#1161=FACE_BOUND('',#4331,.T.);
#1162=FACE_BOUND('',#4332,.T.);
#1163=FACE_BOUND('',#4333,.T.);
#1164=FACE_BOUND('',#4336,.T.);
#1165=FACE_BOUND('',#4337,.T.);
#1166=FACE_BOUND('',#4338,.T.);
#1167=FACE_BOUND('',#4339,.T.);
#1168=FACE_BOUND('',#4340,.T.);
#1169=FACE_BOUND('',#4341,.T.);
#1170=FACE_BOUND('',#4342,.T.);
#1662=PLANE('',#26004);
#1663=PLANE('',#26007);
#1664=PLANE('',#26008);
#1665=PLANE('',#26011);
#1666=PLANE('',#26012);
#1667=PLANE('',#26013);
#2787=FACE_OUTER_BOUND('',#4319,.T.);
#2788=FACE_OUTER_BOUND('',#4320,.T.);
#2789=FACE_OUTER_BOUND('',#4321,.T.);
#2790=FACE_OUTER_BOUND('',#4322,.T.);
#2791=FACE_OUTER_BOUND('',#4323,.T.);
#2792=FACE_OUTER_BOUND('',#4324,.T.);
#2793=FACE_OUTER_BOUND('',#4325,.T.);
#2794=FACE_OUTER_BOUND('',#4326,.T.);
#2795=FACE_OUTER_BOUND('',#4334,.T.);
#2796=FACE_OUTER_BOUND('',#4335,.T.);
#2797=FACE_OUTER_BOUND('',#4343,.T.);
#2798=FACE_OUTER_BOUND('',#4344,.T.);
#2799=FACE_OUTER_BOUND('',#4345,.T.);
#2800=FACE_OUTER_BOUND('',#4346,.T.);
#2801=FACE_OUTER_BOUND('',#4347,.T.);
#4319=EDGE_LOOP('',(#18874,#18875,#18876,#18877));
#4320=EDGE_LOOP('',(#18878,#18879,#18880,#18881));
#4321=EDGE_LOOP('',(#18882,#18883,#18884,#18885));
#4322=EDGE_LOOP('',(#18886,#18887,#18888,#18889));
#4323=EDGE_LOOP('',(#18890,#18891,#18892,#18893));
#4324=EDGE_LOOP('',(#18894,#18895,#18896,#18897));
#4325=EDGE_LOOP('',(#18898,#18899,#18900,#18901));
#4326=EDGE_LOOP('',(#18902,#18903,#18904,#18905,#18906,#18907));
#4327=EDGE_LOOP('',(#18908));
#4328=EDGE_LOOP('',(#18909));
#4329=EDGE_LOOP('',(#18910));
#4330=EDGE_LOOP('',(#18911));
#4331=EDGE_LOOP('',(#18912));
#4332=EDGE_LOOP('',(#18913));
#4333=EDGE_LOOP('',(#18914));
#4334=EDGE_LOOP('',(#18915,#18916,#18917,#18918));
#4335=EDGE_LOOP('',(#18919,#18920,#18921,#18922,#18923,#18924));
#4336=EDGE_LOOP('',(#18925));
#4337=EDGE_LOOP('',(#18926));
#4338=EDGE_LOOP('',(#18927));
#4339=EDGE_LOOP('',(#18928));
#4340=EDGE_LOOP('',(#18929));
#4341=EDGE_LOOP('',(#18930));
#4342=EDGE_LOOP('',(#18931));
#4343=EDGE_LOOP('',(#18932,#18933,#18934,#18935));
#4344=EDGE_LOOP('',(#18936,#18937,#18938,#18939));
#4345=EDGE_LOOP('',(#18940,#18941,#18942,#18943));
#4346=EDGE_LOOP('',(#18944,#18945,#18946,#18947));
#4347=EDGE_LOOP('',(#18948,#18949,#18950,#18951));
#5978=LINE('',#52783,#7945);
#5979=LINE('',#52789,#7946);
#5980=LINE('',#52795,#7947);
#5981=LINE('',#52801,#7948);
#5982=LINE('',#52807,#7949);
#5983=LINE('',#52813,#7950);
#5984=LINE('',#52819,#7951);
#5985=LINE('',#52824,#7952);
#5986=LINE('',#52828,#7953);
#5987=LINE('',#52830,#7954);
#5988=LINE('',#52832,#7955);
#5989=LINE('',#52837,#7956);
#5990=LINE('',#52838,#7957);
#5991=LINE('',#52839,#7958);
#5992=LINE('',#52843,#7959);
#5993=LINE('',#52848,#7960);
#5994=LINE('',#52849,#7961);
#5995=LINE('',#52851,#7962);
#5996=LINE('',#52852,#7963);
#5997=LINE('',#52854,#7964);
#5998=LINE('',#52856,#7965);
#7945=VECTOR('',#30408,2.1);
#7946=VECTOR('',#30415,2.1);
#7947=VECTOR('',#30422,2.1);
#7948=VECTOR('',#30429,2.1);
#7949=VECTOR('',#30436,2.1);
#7950=VECTOR('',#30443,2.1);
#7951=VECTOR('',#30450,14.);
#7952=VECTOR('',#30455,1000.);
#7953=VECTOR('',#30458,1000.);
#7954=VECTOR('',#30459,1000.);
#7955=VECTOR('',#30460,1000.);
#7956=VECTOR('',#30465,1000.);
#7957=VECTOR('',#30466,1000.);
#7958=VECTOR('',#30467,1000.);
#7959=VECTOR('',#30470,1000.);
#7960=VECTOR('',#30475,1000.);
#7961=VECTOR('',#30476,1000.);
#7962=VECTOR('',#30479,1000.);
#7963=VECTOR('',#30480,1000.);
#7964=VECTOR('',#30483,1000.);
#7965=VECTOR('',#30486,1000.);
#9666=CIRCLE('',#25984,2.1);
#9667=CIRCLE('',#25985,2.1);
#9668=CIRCLE('',#25987,2.1);
#9669=CIRCLE('',#25988,2.1);
#9670=CIRCLE('',#25990,2.1);
#9671=CIRCLE('',#25991,2.1);
#9672=CIRCLE('',#25993,2.1);
#9673=CIRCLE('',#25994,2.1);
#9674=CIRCLE('',#25996,2.1);
#9675=CIRCLE('',#25997,2.1);
#9676=CIRCLE('',#25999,2.1);
#9677=CIRCLE('',#26000,2.1);
#9678=CIRCLE('',#26002,14.);
#9679=CIRCLE('',#26003,14.);
#9680=CIRCLE('',#26005,10.);
#9681=CIRCLE('',#26006,10.);
#9682=CIRCLE('',#26009,10.);
#9683=CIRCLE('',#26010,10.);
#11223=VERTEX_POINT('',#52780);
#11224=VERTEX_POINT('',#52782);
#11225=VERTEX_POINT('',#52786);
#11226=VERTEX_POINT('',#52788);
#11227=VERTEX_POINT('',#52792);
#11228=VERTEX_POINT('',#52794);
#11229=VERTEX_POINT('',#52798);
#11230=VERTEX_POINT('',#52800);
#11231=VERTEX_POINT('',#52804);
#11232=VERTEX_POINT('',#52806);
#11233=VERTEX_POINT('',#52810);
#11234=VERTEX_POINT('',#52812);
#11235=VERTEX_POINT('',#52816);
#11236=VERTEX_POINT('',#52818);
#11237=VERTEX_POINT('',#52822);
#11238=VERTEX_POINT('',#52823);
#11239=VERTEX_POINT('',#52825);
#11240=VERTEX_POINT('',#52827);
#11241=VERTEX_POINT('',#52829);
#11242=VERTEX_POINT('',#52831);
#11243=VERTEX_POINT('',#52835);
#11244=VERTEX_POINT('',#52836);
#11245=VERTEX_POINT('',#52841);
#11246=VERTEX_POINT('',#52842);
#11247=VERTEX_POINT('',#52845);
#11248=VERTEX_POINT('',#52847);
#13982=EDGE_CURVE('',#11223,#11223,#9666,.T.);
#13983=EDGE_CURVE('',#11223,#11224,#5978,.T.);
#13984=EDGE_CURVE('',#11224,#11224,#9667,.T.);
#13985=EDGE_CURVE('',#11225,#11225,#9668,.T.);
#13986=EDGE_CURVE('',#11225,#11226,#5979,.T.);
#13987=EDGE_CURVE('',#11226,#11226,#9669,.T.);
#13988=EDGE_CURVE('',#11227,#11227,#9670,.T.);
#13989=EDGE_CURVE('',#11227,#11228,#5980,.T.);
#13990=EDGE_CURVE('',#11228,#11228,#9671,.T.);
#13991=EDGE_CURVE('',#11229,#11229,#9672,.T.);
#13992=EDGE_CURVE('',#11229,#11230,#5981,.T.);
#13993=EDGE_CURVE('',#11230,#11230,#9673,.T.);
#13994=EDGE_CURVE('',#11231,#11231,#9674,.T.);
#13995=EDGE_CURVE('',#11231,#11232,#5982,.T.);
#13996=EDGE_CURVE('',#11232,#11232,#9675,.T.);
#13997=EDGE_CURVE('',#11233,#11233,#9676,.T.);
#13998=EDGE_CURVE('',#11233,#11234,#5983,.T.);
#13999=EDGE_CURVE('',#11234,#11234,#9677,.T.);
#14000=EDGE_CURVE('',#11235,#11235,#9678,.T.);
#14001=EDGE_CURVE('',#11235,#11236,#5984,.T.);
#14002=EDGE_CURVE('',#11236,#11236,#9679,.T.);
#14003=EDGE_CURVE('',#11237,#11238,#5985,.T.);
#14004=EDGE_CURVE('',#11237,#11239,#9680,.T.);
#14005=EDGE_CURVE('',#11240,#11239,#5986,.T.);
#14006=EDGE_CURVE('',#11240,#11241,#5987,.T.);
#14007=EDGE_CURVE('',#11241,#11242,#5988,.T.);
#14008=EDGE_CURVE('',#11242,#11238,#9681,.T.);
#14009=EDGE_CURVE('',#11243,#11244,#5989,.T.);
#14010=EDGE_CURVE('',#11243,#11237,#5990,.T.);
#14011=EDGE_CURVE('',#11238,#11244,#5991,.T.);
#14012=EDGE_CURVE('',#11245,#11246,#5992,.T.);
#14013=EDGE_CURVE('',#11245,#11243,#9682,.T.);
#14014=EDGE_CURVE('',#11244,#11247,#9683,.T.);
#14015=EDGE_CURVE('',#11247,#11248,#5993,.T.);
#14016=EDGE_CURVE('',#11246,#11248,#5994,.T.);
#14017=EDGE_CURVE('',#11248,#11241,#5995,.T.);
#14018=EDGE_CURVE('',#11246,#11240,#5996,.T.);
#14019=EDGE_CURVE('',#11239,#11245,#5997,.T.);
#14020=EDGE_CURVE('',#11247,#11242,#5998,.T.);
#18874=ORIENTED_EDGE('',*,*,#13982,.F.);
#18875=ORIENTED_EDGE('',*,*,#13983,.T.);
#18876=ORIENTED_EDGE('',*,*,#13984,.T.);
#18877=ORIENTED_EDGE('',*,*,#13983,.F.);
#18878=ORIENTED_EDGE('',*,*,#13985,.F.);
#18879=ORIENTED_EDGE('',*,*,#13986,.T.);
#18880=ORIENTED_EDGE('',*,*,#13987,.T.);
#18881=ORIENTED_EDGE('',*,*,#13986,.F.);
#18882=ORIENTED_EDGE('',*,*,#13988,.F.);
#18883=ORIENTED_EDGE('',*,*,#13989,.T.);
#18884=ORIENTED_EDGE('',*,*,#13990,.T.);
#18885=ORIENTED_EDGE('',*,*,#13989,.F.);
#18886=ORIENTED_EDGE('',*,*,#13991,.F.);
#18887=ORIENTED_EDGE('',*,*,#13992,.T.);
#18888=ORIENTED_EDGE('',*,*,#13993,.T.);
#18889=ORIENTED_EDGE('',*,*,#13992,.F.);
#18890=ORIENTED_EDGE('',*,*,#13994,.F.);
#18891=ORIENTED_EDGE('',*,*,#13995,.T.);
#18892=ORIENTED_EDGE('',*,*,#13996,.T.);
#18893=ORIENTED_EDGE('',*,*,#13995,.F.);
#18894=ORIENTED_EDGE('',*,*,#13997,.F.);
#18895=ORIENTED_EDGE('',*,*,#13998,.T.);
#18896=ORIENTED_EDGE('',*,*,#13999,.T.);
#18897=ORIENTED_EDGE('',*,*,#13998,.F.);
#18898=ORIENTED_EDGE('',*,*,#14000,.F.);
#18899=ORIENTED_EDGE('',*,*,#14001,.T.);
#18900=ORIENTED_EDGE('',*,*,#14002,.T.);
#18901=ORIENTED_EDGE('',*,*,#14001,.F.);
#18902=ORIENTED_EDGE('',*,*,#14003,.F.);
#18903=ORIENTED_EDGE('',*,*,#14004,.T.);
#18904=ORIENTED_EDGE('',*,*,#14005,.F.);
#18905=ORIENTED_EDGE('',*,*,#14006,.T.);
#18906=ORIENTED_EDGE('',*,*,#14007,.T.);
#18907=ORIENTED_EDGE('',*,*,#14008,.T.);
#18908=ORIENTED_EDGE('',*,*,#13987,.F.);
#18909=ORIENTED_EDGE('',*,*,#13984,.F.);
#18910=ORIENTED_EDGE('',*,*,#13990,.F.);
#18911=ORIENTED_EDGE('',*,*,#13993,.F.);
#18912=ORIENTED_EDGE('',*,*,#13996,.F.);
#18913=ORIENTED_EDGE('',*,*,#13999,.F.);
#18914=ORIENTED_EDGE('',*,*,#14002,.F.);
#18915=ORIENTED_EDGE('',*,*,#14009,.F.);
#18916=ORIENTED_EDGE('',*,*,#14010,.T.);
#18917=ORIENTED_EDGE('',*,*,#14003,.T.);
#18918=ORIENTED_EDGE('',*,*,#14011,.T.);
#18919=ORIENTED_EDGE('',*,*,#14012,.F.);
#18920=ORIENTED_EDGE('',*,*,#14013,.T.);
#18921=ORIENTED_EDGE('',*,*,#14009,.T.);
#18922=ORIENTED_EDGE('',*,*,#14014,.T.);
#18923=ORIENTED_EDGE('',*,*,#14015,.T.);
#18924=ORIENTED_EDGE('',*,*,#14016,.F.);
#18925=ORIENTED_EDGE('',*,*,#13982,.T.);
#18926=ORIENTED_EDGE('',*,*,#13985,.T.);
#18927=ORIENTED_EDGE('',*,*,#13988,.T.);
#18928=ORIENTED_EDGE('',*,*,#13991,.T.);
#18929=ORIENTED_EDGE('',*,*,#13994,.T.);
#18930=ORIENTED_EDGE('',*,*,#13997,.T.);
#18931=ORIENTED_EDGE('',*,*,#14000,.T.);
#18932=ORIENTED_EDGE('',*,*,#14017,.T.);
#18933=ORIENTED_EDGE('',*,*,#14006,.F.);
#18934=ORIENTED_EDGE('',*,*,#14018,.F.);
#18935=ORIENTED_EDGE('',*,*,#14016,.T.);
#18936=ORIENTED_EDGE('',*,*,#14005,.T.);
#18937=ORIENTED_EDGE('',*,*,#14019,.T.);
#18938=ORIENTED_EDGE('',*,*,#14012,.T.);
#18939=ORIENTED_EDGE('',*,*,#14018,.T.);
#18940=ORIENTED_EDGE('',*,*,#14015,.F.);
#18941=ORIENTED_EDGE('',*,*,#14020,.T.);
#18942=ORIENTED_EDGE('',*,*,#14007,.F.);
#18943=ORIENTED_EDGE('',*,*,#14017,.F.);
#18944=ORIENTED_EDGE('',*,*,#14004,.F.);
#18945=ORIENTED_EDGE('',*,*,#14010,.F.);
#18946=ORIENTED_EDGE('',*,*,#14013,.F.);
#18947=ORIENTED_EDGE('',*,*,#14019,.F.);
#18948=ORIENTED_EDGE('',*,*,#14008,.F.);
#18949=ORIENTED_EDGE('',*,*,#14020,.F.);
#18950=ORIENTED_EDGE('',*,*,#14014,.F.);
#18951=ORIENTED_EDGE('',*,*,#14011,.F.);
#22887=CYLINDRICAL_SURFACE('',#25983,2.1);
#22888=CYLINDRICAL_SURFACE('',#25986,2.1);
#22889=CYLINDRICAL_SURFACE('',#25989,2.1);
#22890=CYLINDRICAL_SURFACE('',#25992,2.1);
#22891=CYLINDRICAL_SURFACE('',#25995,2.1);
#22892=CYLINDRICAL_SURFACE('',#25998,2.1);
#22893=CYLINDRICAL_SURFACE('',#26001,14.);
#22894=CYLINDRICAL_SURFACE('',#26014,10.);
#22895=CYLINDRICAL_SURFACE('',#26015,10.);
#23779=ADVANCED_FACE('',(#2787),#22887,.F.);
#23780=ADVANCED_FACE('',(#2788),#22888,.F.);
#23781=ADVANCED_FACE('',(#2789),#22889,.F.);
#23782=ADVANCED_FACE('',(#2790),#22890,.F.);
#23783=ADVANCED_FACE('',(#2791),#22891,.F.);
#23784=ADVANCED_FACE('',(#2792),#22892,.F.);
#23785=ADVANCED_FACE('',(#2793),#22893,.F.);
#23786=ADVANCED_FACE('',(#2794,#1157,#1158,#1159,#1160,#1161,#1162,#1163),
#1662,.F.);
#23787=ADVANCED_FACE('',(#2795),#1663,.F.);
#23788=ADVANCED_FACE('',(#2796,#1164,#1165,#1166,#1167,#1168,#1169,#1170),
#1664,.F.);
#23789=ADVANCED_FACE('',(#2797),#1665,.F.);
#23790=ADVANCED_FACE('',(#2798),#1666,.F.);
#23791=ADVANCED_FACE('',(#2799),#1667,.T.);
#23792=ADVANCED_FACE('',(#2800),#22894,.T.);
#23793=ADVANCED_FACE('',(#2801),#22895,.T.);
#24544=CLOSED_SHELL('',(#23779,#23780,#23781,#23782,#23783,#23784,#23785,
#23786,#23787,#23788,#23789,#23790,#23791,#23792,#23793));
#25982=AXIS2_PLACEMENT_3D('',#52778,#30402,#30403);
#25983=AXIS2_PLACEMENT_3D('',#52779,#30404,#30405);
#25984=AXIS2_PLACEMENT_3D('',#52781,#30406,#30407);
#25985=AXIS2_PLACEMENT_3D('',#52784,#30409,#30410);
#25986=AXIS2_PLACEMENT_3D('',#52785,#30411,#30412);
#25987=AXIS2_PLACEMENT_3D('',#52787,#30413,#30414);
#25988=AXIS2_PLACEMENT_3D('',#52790,#30416,#30417);
#25989=AXIS2_PLACEMENT_3D('',#52791,#30418,#30419);
#25990=AXIS2_PLACEMENT_3D('',#52793,#30420,#30421);
#25991=AXIS2_PLACEMENT_3D('',#52796,#30423,#30424);
#25992=AXIS2_PLACEMENT_3D('',#52797,#30425,#30426);
#25993=AXIS2_PLACEMENT_3D('',#52799,#30427,#30428);
#25994=AXIS2_PLACEMENT_3D('',#52802,#30430,#30431);
#25995=AXIS2_PLACEMENT_3D('',#52803,#30432,#30433);
#25996=AXIS2_PLACEMENT_3D('',#52805,#30434,#30435);
#25997=AXIS2_PLACEMENT_3D('',#52808,#30437,#30438);
#25998=AXIS2_PLACEMENT_3D('',#52809,#30439,#30440);
#25999=AXIS2_PLACEMENT_3D('',#52811,#30441,#30442);
#26000=AXIS2_PLACEMENT_3D('',#52814,#30444,#30445);
#26001=AXIS2_PLACEMENT_3D('',#52815,#30446,#30447);
#26002=AXIS2_PLACEMENT_3D('',#52817,#30448,#30449);
#26003=AXIS2_PLACEMENT_3D('',#52820,#30451,#30452);
#26004=AXIS2_PLACEMENT_3D('',#52821,#30453,#30454);
#26005=AXIS2_PLACEMENT_3D('',#52826,#30456,#30457);
#26006=AXIS2_PLACEMENT_3D('',#52833,#30461,#30462);
#26007=AXIS2_PLACEMENT_3D('',#52834,#30463,#30464);
#26008=AXIS2_PLACEMENT_3D('',#52840,#30468,#30469);
#26009=AXIS2_PLACEMENT_3D('',#52844,#30471,#30472);
#26010=AXIS2_PLACEMENT_3D('',#52846,#30473,#30474);
#26011=AXIS2_PLACEMENT_3D('',#52850,#30477,#30478);
#26012=AXIS2_PLACEMENT_3D('',#52853,#30481,#30482);
#26013=AXIS2_PLACEMENT_3D('',#52855,#30484,#30485);
#26014=AXIS2_PLACEMENT_3D('',#52857,#30487,#30488);
#26015=AXIS2_PLACEMENT_3D('',#52858,#30489,#30490);
#30402=DIRECTION('axis',(0.,0.,1.));
#30403=DIRECTION('refdir',(1.,0.,0.));
#30404=DIRECTION('center_axis',(0.,-1.,0.));
#30405=DIRECTION('ref_axis',(0.,0.,-1.));
#30406=DIRECTION('center_axis',(0.,-1.,0.));
#30407=DIRECTION('ref_axis',(0.,0.,-1.));
#30408=DIRECTION('',(0.,-1.,0.));
#30409=DIRECTION('center_axis',(0.,-1.,0.));
#30410=DIRECTION('ref_axis',(0.,0.,-1.));
#30411=DIRECTION('center_axis',(0.,-1.,0.));
#30412=DIRECTION('ref_axis',(0.,0.,-1.));
#30413=DIRECTION('center_axis',(0.,-1.,0.));
#30414=DIRECTION('ref_axis',(0.,0.,-1.));
#30415=DIRECTION('',(0.,-1.,0.));
#30416=DIRECTION('center_axis',(0.,-1.,0.));
#30417=DIRECTION('ref_axis',(0.,0.,-1.));
#30418=DIRECTION('center_axis',(0.,-1.,0.));
#30419=DIRECTION('ref_axis',(0.,0.,-1.));
#30420=DIRECTION('center_axis',(0.,-1.,0.));
#30421=DIRECTION('ref_axis',(0.,0.,-1.));
#30422=DIRECTION('',(0.,-1.,0.));
#30423=DIRECTION('center_axis',(0.,-1.,0.));
#30424=DIRECTION('ref_axis',(0.,0.,-1.));
#30425=DIRECTION('center_axis',(0.,-1.,0.));
#30426=DIRECTION('ref_axis',(0.,0.,-1.));
#30427=DIRECTION('center_axis',(0.,-1.,0.));
#30428=DIRECTION('ref_axis',(0.,0.,-1.));
#30429=DIRECTION('',(0.,-1.,0.));
#30430=DIRECTION('center_axis',(0.,-1.,0.));
#30431=DIRECTION('ref_axis',(0.,0.,-1.));
#30432=DIRECTION('center_axis',(0.,-1.,0.));
#30433=DIRECTION('ref_axis',(0.,0.,-1.));
#30434=DIRECTION('center_axis',(0.,-1.,0.));
#30435=DIRECTION('ref_axis',(0.,0.,-1.));
#30436=DIRECTION('',(0.,-1.,0.));
#30437=DIRECTION('center_axis',(0.,-1.,0.));
#30438=DIRECTION('ref_axis',(0.,0.,-1.));
#30439=DIRECTION('center_axis',(0.,-1.,0.));
#30440=DIRECTION('ref_axis',(0.,0.,-1.));
#30441=DIRECTION('center_axis',(0.,-1.,0.));
#30442=DIRECTION('ref_axis',(0.,0.,-1.));
#30443=DIRECTION('',(0.,-1.,0.));
#30444=DIRECTION('center_axis',(0.,-1.,0.));
#30445=DIRECTION('ref_axis',(0.,0.,-1.));
#30446=DIRECTION('center_axis',(0.,-1.,0.));
#30447=DIRECTION('ref_axis',(0.,0.,-1.));
#30448=DIRECTION('center_axis',(0.,-1.,0.));
#30449=DIRECTION('ref_axis',(0.,0.,-1.));
#30450=DIRECTION('',(0.,-1.,0.));
#30451=DIRECTION('center_axis',(0.,-1.,0.));
#30452=DIRECTION('ref_axis',(0.,0.,-1.));
#30453=DIRECTION('center_axis',(0.,1.,0.));
#30454=DIRECTION('ref_axis',(0.,0.,1.));
#30455=DIRECTION('',(0.,0.,-1.));
#30456=DIRECTION('center_axis',(0.,-1.,0.));
#30457=DIRECTION('ref_axis',(0.,0.,1.));
#30458=DIRECTION('',(1.,0.,0.));
#30459=DIRECTION('',(0.,0.,-1.));
#30460=DIRECTION('',(1.,0.,0.));
#30461=DIRECTION('center_axis',(0.,-1.,0.));
#30462=DIRECTION('ref_axis',(0.,0.,1.));
#30463=DIRECTION('center_axis',(-1.,0.,0.));
#30464=DIRECTION('ref_axis',(0.,0.,1.));
#30465=DIRECTION('',(0.,0.,-1.));
#30466=DIRECTION('',(0.,-1.,0.));
#30467=DIRECTION('',(0.,1.,0.));
#30468=DIRECTION('center_axis',(0.,-1.,0.));
#30469=DIRECTION('ref_axis',(0.,0.,-1.));
#30470=DIRECTION('',(-1.,0.,0.));
#30471=DIRECTION('center_axis',(0.,1.,0.));
#30472=DIRECTION('ref_axis',(0.,0.,-1.));
#30473=DIRECTION('center_axis',(0.,1.,0.));
#30474=DIRECTION('ref_axis',(0.,0.,-1.));
#30475=DIRECTION('',(-1.,0.,0.));
#30476=DIRECTION('',(0.,0.,-1.));
#30477=DIRECTION('center_axis',(1.,0.,0.));
#30478=DIRECTION('ref_axis',(0.,0.,-1.));
#30479=DIRECTION('',(0.,-1.,0.));
#30480=DIRECTION('',(0.,-1.,0.));
#30481=DIRECTION('center_axis',(0.,0.,-1.));
#30482=DIRECTION('ref_axis',(-1.,0.,0.));
#30483=DIRECTION('',(0.,1.,0.));
#30484=DIRECTION('center_axis',(0.,0.,-1.));
#30485=DIRECTION('ref_axis',(-1.,0.,0.));
#30486=DIRECTION('',(0.,-1.,0.));
#30487=DIRECTION('center_axis',(0.,1.,0.));
#30488=DIRECTION('ref_axis',(0.,0.,1.));
#30489=DIRECTION('center_axis',(0.,-1.,0.));
#30490=DIRECTION('ref_axis',(0.,0.,-1.));
#52778=CARTESIAN_POINT('',(0.,0.,0.));
#52779=CARTESIAN_POINT('Origin',(-3.43502884254442,-7.,13.4350288425444));
#52780=CARTESIAN_POINT('',(-3.43502884254442,7.,15.5350288425444));
#52781=CARTESIAN_POINT('Origin',(-3.43502884254442,7.,13.4350288425444));
#52782=CARTESIAN_POINT('',(-3.43502884254442,-7.,15.5350288425444));
#52783=CARTESIAN_POINT('',(-3.43502884254442,-7.,15.5350288425444));
#52784=CARTESIAN_POINT('Origin',(-3.43502884254442,-7.,13.4350288425444));
#52785=CARTESIAN_POINT('Origin',(10.,-7.,19.));
#52786=CARTESIAN_POINT('',(10.,7.,21.1));
#52787=CARTESIAN_POINT('Origin',(10.,7.,19.));
#52788=CARTESIAN_POINT('',(10.,-7.,21.1));
#52789=CARTESIAN_POINT('',(10.,-7.,21.1));
#52790=CARTESIAN_POINT('Origin',(10.,-7.,19.));
#52791=CARTESIAN_POINT('Origin',(23.4350288425443,-7.,13.4350288425445));
#52792=CARTESIAN_POINT('',(23.4350288425443,7.,15.5350288425445));
#52793=CARTESIAN_POINT('Origin',(23.4350288425443,7.,13.4350288425445));
#52794=CARTESIAN_POINT('',(23.4350288425443,-7.,15.5350288425445));
#52795=CARTESIAN_POINT('',(23.4350288425443,-7.,15.5350288425445));
#52796=CARTESIAN_POINT('Origin',(23.4350288425443,-7.,13.4350288425445));
#52797=CARTESIAN_POINT('Origin',(-3.43502884254442,-7.,-13.4350288425444));
#52798=CARTESIAN_POINT('',(-3.43502884254442,7.,-11.3350288425444));
#52799=CARTESIAN_POINT('Origin',(-3.43502884254442,7.,-13.4350288425444));
#52800=CARTESIAN_POINT('',(-3.43502884254442,-7.,-11.3350288425444));
#52801=CARTESIAN_POINT('',(-3.43502884254442,-7.,-11.3350288425444));
#52802=CARTESIAN_POINT('Origin',(-3.43502884254442,-7.,-13.4350288425444));
#52803=CARTESIAN_POINT('Origin',(10.,-7.,-19.));
#52804=CARTESIAN_POINT('',(10.,7.,-16.9));
#52805=CARTESIAN_POINT('Origin',(10.,7.,-19.));
#52806=CARTESIAN_POINT('',(10.,-7.,-16.9));
#52807=CARTESIAN_POINT('',(10.,-7.,-16.9));
#52808=CARTESIAN_POINT('Origin',(10.,-7.,-19.));
#52809=CARTESIAN_POINT('Origin',(23.4350288425443,-7.,-13.4350288425445));
#52810=CARTESIAN_POINT('',(23.4350288425443,7.,-11.3350288425445));
#52811=CARTESIAN_POINT('Origin',(23.4350288425443,7.,-13.4350288425445));
#52812=CARTESIAN_POINT('',(23.4350288425443,-7.,-11.3350288425445));
#52813=CARTESIAN_POINT('',(23.4350288425443,-7.,-11.3350288425445));
#52814=CARTESIAN_POINT('Origin',(23.4350288425443,-7.,-13.4350288425445));
#52815=CARTESIAN_POINT('Origin',(10.,7.,0.));
#52816=CARTESIAN_POINT('',(10.,7.,14.));
#52817=CARTESIAN_POINT('Origin',(10.,7.,0.));
#52818=CARTESIAN_POINT('',(10.,-7.,14.));
#52819=CARTESIAN_POINT('',(10.,7.,14.));
#52820=CARTESIAN_POINT('Origin',(10.,-7.,0.));
#52821=CARTESIAN_POINT('Origin',(-32.,-7.,35.));
#52822=CARTESIAN_POINT('',(32.,-7.,25.));
#52823=CARTESIAN_POINT('',(32.,-7.,-25.));
#52824=CARTESIAN_POINT('',(32.,-7.,35.));
#52825=CARTESIAN_POINT('',(22.,-7.,35.));
#52826=CARTESIAN_POINT('Origin',(22.,-7.,25.));
#52827=CARTESIAN_POINT('',(-32.,-7.,35.));
#52828=CARTESIAN_POINT('',(-32.,-7.,35.));
#52829=CARTESIAN_POINT('',(-32.,-7.,-35.));
#52830=CARTESIAN_POINT('',(-32.,-7.,35.));
#52831=CARTESIAN_POINT('',(22.,-7.,-35.));
#52832=CARTESIAN_POINT('',(-32.,-7.,-35.));
#52833=CARTESIAN_POINT('Origin',(22.,-7.,-25.));
#52834=CARTESIAN_POINT('Origin',(32.,-7.,35.));
#52835=CARTESIAN_POINT('',(32.,7.,25.));
#52836=CARTESIAN_POINT('',(32.,7.,-25.));
#52837=CARTESIAN_POINT('',(32.,7.,35.));
#52838=CARTESIAN_POINT('',(32.,-7.,25.));
#52839=CARTESIAN_POINT('',(32.,7.,-25.));
#52840=CARTESIAN_POINT('Origin',(-32.,7.,35.));
#52841=CARTESIAN_POINT('',(22.,7.,35.));
#52842=CARTESIAN_POINT('',(-32.,7.,35.));
#52843=CARTESIAN_POINT('',(-32.,7.,35.));
#52844=CARTESIAN_POINT('Origin',(22.,7.,25.));
#52845=CARTESIAN_POINT('',(22.,7.,-35.));
#52846=CARTESIAN_POINT('Origin',(22.,7.,-25.));
#52847=CARTESIAN_POINT('',(-32.,7.,-35.));
#52848=CARTESIAN_POINT('',(-32.,7.,-35.));
#52849=CARTESIAN_POINT('',(-32.,7.,35.));
#52850=CARTESIAN_POINT('Origin',(-32.,-7.,35.));
#52851=CARTESIAN_POINT('',(-32.,-7.,-35.));
#52852=CARTESIAN_POINT('',(-32.,-7.,35.));
#52853=CARTESIAN_POINT('Origin',(0.,0.,35.));
#52854=CARTESIAN_POINT('',(22.,0.,35.));
#52855=CARTESIAN_POINT('Origin',(0.,0.,-35.));
#52856=CARTESIAN_POINT('',(22.,-7.,-35.));
#52857=CARTESIAN_POINT('Origin',(22.,0.,25.));
#52858=CARTESIAN_POINT('Origin',(22.,-7.,-25.));
#57026=UNCERTAINTY_MEASURE_WITH_UNIT(LENGTH_MEASURE(0.01),#57080,
'DISTANCE_ACCURACY_VALUE',
'Maximum model space distance between geometric entities at asserted c
onnectivities');
#57040=UNCERTAINTY_MEASURE_WITH_UNIT(LENGTH_MEASURE(0.01),#57080,
'DISTANCE_ACCURACY_VALUE',
'Maximum model space distance between geometric entities at asserted c
onnectivities');
#57065=(
GEOMETRIC_REPRESENTATION_CONTEXT(3)
GLOBAL_UNCERTAINTY_ASSIGNED_CONTEXT((#57026))
GLOBAL_UNIT_ASSIGNED_CONTEXT((#57080,#57082,#57083))
REPRESENTATION_CONTEXT('','3D')
);
#57079=(
GEOMETRIC_REPRESENTATION_CONTEXT(3)
GLOBAL_UNCERTAINTY_ASSIGNED_CONTEXT((#57040))
GLOBAL_UNIT_ASSIGNED_CONTEXT((#57080,#57082,#57083))
REPRESENTATION_CONTEXT('','3D')
);
#57080=(
LENGTH_UNIT()
NAMED_UNIT(*)
SI_UNIT(.MILLI.,.METRE.)
);
#57082=(
NAMED_UNIT(*)
PLANE_ANGLE_UNIT()
SI_UNIT($,.RADIAN.)
);
#57083=(
NAMED_UNIT(*)
SI_UNIT($,.STERADIAN.)
SOLID_ANGLE_UNIT()
);
#57108=SHAPE_DEFINITION_REPRESENTATION(#57160,#57273);
#57160=PRODUCT_DEFINITION_SHAPE('',$,#57312);
#57273=SHAPE_REPRESENTATION('',(#25982),#57065);
#57287=PRODUCT_DEFINITION_CONTEXT('part definition',#57403,'design');
#57312=PRODUCT_DEFINITION('Ball Screw Support Bracket',
'Ball Screw Support Bracket',#57350,#57287);
#57350=PRODUCT_DEFINITION_FORMATION('',$,#57429);
#57403=APPLICATION_CONTEXT(
'Core Data for Automotive Mechanical Design Process');
#57404=PRODUCT_CONTEXT('part definition',#57403,'mechanical');
#57429=PRODUCT('Ball Screw Support Bracket',
'Ball Screw Support Bracket',$,(#57404));
#57444=PRESENTATION_STYLE_ASSIGNMENT((#57446));
#57446=SURFACE_STYLE_USAGE(.BOTH.,#57448);
#57448=SURFACE_SIDE_STYLE('',(#57450));
#57450=SURFACE_STYLE_FILL_AREA(#57452);
#57452=FILL_AREA_STYLE('Opaque(202,209,238)',(#57454));
#57454=FILL_AREA_STYLE_COLOUR('Opaque(202,209,238)',#57456);
#57456=COLOUR_RGB('Opaque(202,209,238)',0.792156862745098,0.819607843137255,
0.933333333333333);
ENDSEC;
END-ISO-10303-21;
